ISO-10303-21;
HEADER;
/* Generated by software containing ST-Developer
 * from STEP Tools, Inc. (www.steptools.com) 
 */

FILE_DESCRIPTION(
/* description */ (''),
/* implementation_level */ '2;1');

FILE_NAME(
/* name */ 'ASME B18.22.1 Plain Washer No.6 Narrow.step',
/* time_stamp */ '2026-10-15T13:29:10-07:00',
/* author */ (''),
/* organization */ (''),
/* preprocessor_version */ 'ST-DEVELOPER v20.2',
/* originating_system */ 'Autodesk Translation Framework v15.15.0.0',
/* authorisation */ '');

FILE_SCHEMA (('AUTOMOTIVE_DESIGN { 1 0 10303 214 3 1 1 }'));
ENDSEC;

DATA;
#10=MECHANICAL_DESIGN_GEOMETRIC_PRESENTATION_REPRESENTATION('',(#945),#83219);
#917=SHAPE_REPRESENTATION_RELATIONSHIP('SRR','None',#83312,#931);
#931=ADVANCED_BREP_SHAPE_REPRESENTATION('',(#959),#83217);
#945=STYLED_ITEM('',(#83391),#959);
#959=MANIFOLD_SOLID_BREP('Body1',#26941);
#1117=FACE_BOUND('',#5251,.T.);
#1118=FACE_BOUND('',#5255,.T.);
#2130=PLANE('',#29175);
#2131=PLANE('',#29181);
#2352=CYLINDRICAL_SURFACE('',#29177,4.7625);
#2353=CYLINDRICAL_SURFACE('',#29183,1.98119999999999);
#3714=FACE_OUTER_BOUND('',#5249,.T.);
#3715=FACE_OUTER_BOUND('',#5250,.T.);
#3716=FACE_OUTER_BOUND('',#5252,.T.);
#3717=FACE_OUTER_BOUND('',#5253,.T.);
#3718=FACE_OUTER_BOUND('',#5254,.T.);
#3719=FACE_OUTER_BOUND('',#5256,.T.);
#5249=EDGE_LOOP('',(#25364,#25365,#25366,#25367));
#5250=EDGE_LOOP('',(#25368));
#5251=EDGE_LOOP('',(#25369));
#5252=EDGE_LOOP('',(#25370,#25371,#25372,#25373));
#5253=EDGE_LOOP('',(#25374,#25375,#25376,#25377));
#5254=EDGE_LOOP('',(#25378));
#5255=EDGE_LOOP('',(#25379));
#5256=EDGE_LOOP('',(#25380,#25381,#25382,#25383));
#7766=LINE('',#83042,#10277);
#7767=LINE('',#83050,#10278);
#7768=LINE('',#83053,#10279);
#7769=LINE('',#83059,#10280);
#10277=VECTOR('',#35896,2.0312);
#10278=VECTOR('',#35907,4.7625);
#10279=VECTOR('',#35910,4.6875);
#10280=VECTOR('',#35919,1.98119999999999);
#11036=CIRCLE('',#29173,1.98119999999999);
#11037=CIRCLE('',#29174,2.08119999999999);
#11038=CIRCLE('',#29176,4.7625);
#11039=CIRCLE('',#29178,4.7625);
#11040=CIRCLE('',#29180,4.6125);
#11041=CIRCLE('',#29182,1.98119999999999);
#13627=VERTEX_POINT('',#83039);
#13628=VERTEX_POINT('',#83041);
#13629=VERTEX_POINT('',#83045);
#13630=VERTEX_POINT('',#83048);
#13631=VERTEX_POINT('',#83052);
#13632=VERTEX_POINT('',#83056);
#17543=EDGE_CURVE('',#13627,#13627,#11036,.T.);
#17544=EDGE_CURVE('',#13627,#13628,#7766,.T.);
#17545=EDGE_CURVE('',#13628,#13628,#11037,.T.);
#17546=EDGE_CURVE('',#13629,#13629,#11038,.T.);
#17547=EDGE_CURVE('',#13630,#13630,#11039,.T.);
#17548=EDGE_CURVE('',#13630,#13629,#7767,.T.);
#17549=EDGE_CURVE('',#13630,#13631,#7768,.T.);
#17550=EDGE_CURVE('',#13631,#13631,#11040,.T.);
#17551=EDGE_CURVE('',#13632,#13632,#11041,.T.);
#17552=EDGE_CURVE('',#13627,#13632,#7769,.T.);
#25364=ORIENTED_EDGE('',*,*,#17543,.T.);
#25365=ORIENTED_EDGE('',*,*,#17544,.T.);
#25366=ORIENTED_EDGE('',*,*,#17545,.F.);
#25367=ORIENTED_EDGE('',*,*,#17544,.F.);
#25368=ORIENTED_EDGE('',*,*,#17546,.F.);
#25369=ORIENTED_EDGE('',*,*,#17545,.T.);
#25370=ORIENTED_EDGE('',*,*,#17547,.F.);
#25371=ORIENTED_EDGE('',*,*,#17548,.T.);
#25372=ORIENTED_EDGE('',*,*,#17546,.T.);
#25373=ORIENTED_EDGE('',*,*,#17548,.F.);
#25374=ORIENTED_EDGE('',*,*,#17547,.T.);
#25375=ORIENTED_EDGE('',*,*,#17549,.T.);
#25376=ORIENTED_EDGE('',*,*,#17550,.F.);
#25377=ORIENTED_EDGE('',*,*,#17549,.F.);
#25378=ORIENTED_EDGE('',*,*,#17550,.T.);
#25379=ORIENTED_EDGE('',*,*,#17551,.F.);
#25380=ORIENTED_EDGE('',*,*,#17543,.F.);
#25381=ORIENTED_EDGE('',*,*,#17552,.T.);
#25382=ORIENTED_EDGE('',*,*,#17551,.T.);
#25383=ORIENTED_EDGE('',*,*,#17552,.F.);
#25545=CONICAL_SURFACE('',#29172,2.0312,0.785398163397493);
#25546=CONICAL_SURFACE('',#29179,4.6875,0.785398163397478);
#26907=ADVANCED_FACE('',(#3714),#25545,.F.);
#26908=ADVANCED_FACE('',(#3715,#1117),#2130,.T.);
#26909=ADVANCED_FACE('',(#3716),#2352,.T.);
#26910=ADVANCED_FACE('',(#3717),#25546,.T.);
#26911=ADVANCED_FACE('',(#3718,#1118),#2131,.T.);
#26912=ADVANCED_FACE('',(#3719),#2353,.F.);
#26941=CLOSED_SHELL('',(#26907,#26908,#26909,#26910,#26911,#26912));
#29171=AXIS2_PLACEMENT_3D('',#83037,#35890,#35891);
#29172=AXIS2_PLACEMENT_3D('',#83038,#35892,#35893);
#29173=AXIS2_PLACEMENT_3D('',#83040,#35894,#35895);
#29174=AXIS2_PLACEMENT_3D('',#83043,#35897,#35898);
#29175=AXIS2_PLACEMENT_3D('',#83044,#35899,#35900);
#29176=AXIS2_PLACEMENT_3D('',#83046,#35901,#35902);
#29177=AXIS2_PLACEMENT_3D('',#83047,#35903,#35904);
#29178=AXIS2_PLACEMENT_3D('',#83049,#35905,#35906);
#29179=AXIS2_PLACEMENT_3D('',#83051,#35908,#35909);
#29180=AXIS2_PLACEMENT_3D('',#83054,#35911,#35912);
#29181=AXIS2_PLACEMENT_3D('',#83055,#35913,#35914);
#29182=AXIS2_PLACEMENT_3D('',#83057,#35915,#35916);
#29183=AXIS2_PLACEMENT_3D('',#83058,#35917,#35918);
#35890=DIRECTION('axis',(0.,0.,1.));
#35891=DIRECTION('refdir',(1.,0.,0.));
#35892=DIRECTION('center_axis',(0.,1.,0.));
#35893=DIRECTION('ref_axis',(1.,0.,0.));
#35894=DIRECTION('center_axis',(0.,-1.,0.));
#35895=DIRECTION('ref_axis',(1.,0.,0.));
#35896=DIRECTION('',(-0.707106781186579,0.707106781186516,8.65956056235532E-17));
#35897=DIRECTION('center_axis',(0.,-1.,0.));
#35898=DIRECTION('ref_axis',(1.,0.,0.));
#35899=DIRECTION('center_axis',(0.,1.,0.));
#35900=DIRECTION('ref_axis',(0.,0.,1.));
#35901=DIRECTION('center_axis',(0.,-1.,0.));
#35902=DIRECTION('ref_axis',(1.,0.,0.));
#35903=DIRECTION('center_axis',(0.,-1.,0.));
#35904=DIRECTION('ref_axis',(1.,0.,0.));
#35905=DIRECTION('center_axis',(0.,-1.,0.));
#35906=DIRECTION('ref_axis',(1.,0.,0.));
#35907=DIRECTION('',(0.,1.,0.));
#35908=DIRECTION('center_axis',(0.,1.,0.));
#35909=DIRECTION('ref_axis',(1.,0.,0.));
#35910=DIRECTION('',(0.707106781186568,-0.707106781186526,-8.65956056235519E-17));
#35911=DIRECTION('center_axis',(0.,-1.,0.));
#35912=DIRECTION('ref_axis',(1.,0.,0.));
#35913=DIRECTION('center_axis',(0.,-1.,0.));
#35914=DIRECTION('ref_axis',(0.,0.,-1.));
#35915=DIRECTION('center_axis',(0.,-1.,0.));
#35916=DIRECTION('ref_axis',(1.,0.,0.));
#35917=DIRECTION('center_axis',(0.,-1.,0.));
#35918=DIRECTION('ref_axis',(1.,0.,0.));
#35919=DIRECTION('',(0.,-1.,0.));
#83037=CARTESIAN_POINT('',(0.,0.,0.));
#83038=CARTESIAN_POINT('Origin',(88.011,65.0396,12.066));
#83039=CARTESIAN_POINT('',(86.0298,64.9896,12.066));
#83040=CARTESIAN_POINT('Origin',(88.011,64.9896,12.066));
#83041=CARTESIAN_POINT('',(85.9298,65.0896,12.066));
#83042=CARTESIAN_POINT('',(85.9798,65.0396,12.066));
#83043=CARTESIAN_POINT('Origin',(88.011,65.0896,12.066));
#83044=CARTESIAN_POINT('Origin',(92.7735,65.0896,12.066));
#83045=CARTESIAN_POINT('',(83.2485,65.0896,12.066));
#83046=CARTESIAN_POINT('Origin',(88.011,65.0896,12.066));
#83047=CARTESIAN_POINT('Origin',(88.011,64.5423,12.066));
#83048=CARTESIAN_POINT('',(83.2485,63.995,12.066));
#83049=CARTESIAN_POINT('Origin',(88.011,63.995,12.066));
#83050=CARTESIAN_POINT('',(83.2485,64.5423,12.066));
#83051=CARTESIAN_POINT('Origin',(88.011,63.92,12.066));
#83052=CARTESIAN_POINT('',(83.3985,63.845,12.066));
#83053=CARTESIAN_POINT('',(83.3235,63.92,12.066));
#83054=CARTESIAN_POINT('Origin',(88.011,63.845,12.066));
#83055=CARTESIAN_POINT('Origin',(89.9922,63.845,12.066));
#83056=CARTESIAN_POINT('',(86.0298,63.845,12.066));
#83057=CARTESIAN_POINT('Origin',(88.011,63.845,12.066));
#83058=CARTESIAN_POINT('Origin',(88.011,64.4173,12.066));
#83059=CARTESIAN_POINT('',(86.0298,64.4173,12.066));
#83201=UNCERTAINTY_MEASURE_WITH_UNIT(LENGTH_MEASURE(0.01),#83220,
'DISTANCE_ACCURACY_VALUE',
'Maximum model space distance between geometric entities at asserted c
onnectivities');
#83203=UNCERTAINTY_MEASURE_WITH_UNIT(LENGTH_MEASURE(0.01),#83220,
'DISTANCE_ACCURACY_VALUE',
'Maximum model space distance between geometric entities at asserted c
onnectivities');
#83217=(
GEOMETRIC_REPRESENTATION_CONTEXT(3)
GLOBAL_UNCERTAINTY_ASSIGNED_CONTEXT((#83201))
GLOBAL_UNIT_ASSIGNED_CONTEXT((#83220,#83222,#83223))
REPRESENTATION_CONTEXT('','3D')
);
#83219=(
GEOMETRIC_REPRESENTATION_CONTEXT(3)
GLOBAL_UNCERTAINTY_ASSIGNED_CONTEXT((#83203))
GLOBAL_UNIT_ASSIGNED_CONTEXT((#83220,#83222,#83223))
REPRESENTATION_CONTEXT('','3D')
);
#83220=(
LENGTH_UNIT()
NAMED_UNIT(*)
SI_UNIT(.MILLI.,.METRE.)
);
#83222=(
NAMED_UNIT(*)
PLANE_ANGLE_UNIT()
SI_UNIT($,.RADIAN.)
);
#83223=(
NAMED_UNIT(*)
SI_UNIT($,.STERADIAN.)
SOLID_ANGLE_UNIT()
);
#83237=SHAPE_DEFINITION_REPRESENTATION(#83252,#83312);
#83252=PRODUCT_DEFINITION_SHAPE('',$,#83328);
#83312=SHAPE_REPRESENTATION('',(#29171),#83217);
#83314=PRODUCT_DEFINITION_CONTEXT('part definition',#83361,'design');
#83328=PRODUCT_DEFINITION('ASME B18.22.1 Plain Washer No.6 Narrow',
'ASME B18.22.1 Plain Washer No.6 Narrow',#83343,#83314);
#83343=PRODUCT_DEFINITION_FORMATION('',$,#83376);
#83361=APPLICATION_CONTEXT(
'Core Data for Automotive Mechanical Design Process');
#83362=PRODUCT_CONTEXT('part definition',#83361,'mechanical');
#83376=PRODUCT('ASME B18.22.1 Plain Washer No.6 Narrow',
'ASME B18.22.1 Plain Washer No.6 Narrow',$,(#83362));
#83391=PRESENTATION_STYLE_ASSIGNMENT((#83406));
#83406=SURFACE_STYLE_USAGE(.BOTH.,#83421);
#83421=SURFACE_SIDE_STYLE('',(#83436));
#83436=SURFACE_STYLE_FILL_AREA(#83451);
#83451=FILL_AREA_STYLE('Opaque(234,236,239)',(#83466));
#83466=FILL_AREA_STYLE_COLOUR('Opaque(234,236,239)',#83481);
#83481=COLOUR_RGB('Opaque(234,236,239)', 0.66274510, 0.83137255, 0.94901961);
ENDSEC;
END-ISO-10303-21;
